ISO-10303-21;
HEADER;
/* Generated by software containing ST-Developer
 * from STEP Tools, Inc. (www.steptools.com) 
 */

FILE_DESCRIPTION(
/* description */ ('Overhung pulley bearing cartridge'),
/* implementation_level */ '2;1');

FILE_NAME(
/* name */ 'Socket Set Screw - M5x8.step',
/* time_stamp */ '2026-10-28T03:22:33-07:00',
/* author */ (''),
/* organization */ (''),
/* preprocessor_version */ 'ST-DEVELOPER v20.2',
/* originating_system */ 'Autodesk Translation Framework v15.17.0.0',
/* authorisation */ '');

FILE_SCHEMA (('AUTOMOTIVE_DESIGN { 1 0 10303 214 3 1 1 }'));
ENDSEC;

DATA;
#10=MECHANICAL_DESIGN_GEOMETRIC_PRESENTATION_REPRESENTATION('',(#312),#10963);
#235=CONICAL_SURFACE('',#6671,0.235,0.785398163397448);
#236=CONICAL_SURFACE('',#6675,0.2125,0.785398163397448);
#260=SHAPE_REPRESENTATION_RELATIONSHIP('SRR','None',#11082,#282);
#282=ADVANCED_BREP_SHAPE_REPRESENTATION('',(#340),#10962);
#312=STYLED_ITEM('',(#11260),#340);
#340=MANIFOLD_SOLID_BREP('Body1',#5681);
#433=FACE_BOUND('',#1323,.T.);
#568=PLANE('',#6662);
#569=PLANE('',#6663);
#570=PLANE('',#6664);
#571=PLANE('',#6665);
#572=PLANE('',#6666);
#573=PLANE('',#6667);
#574=PLANE('',#6668);
#575=PLANE('',#6669);
#576=PLANE('',#6677);
#894=FACE_OUTER_BOUND('',#1315,.T.);
#895=FACE_OUTER_BOUND('',#1316,.T.);
#896=FACE_OUTER_BOUND('',#1317,.T.);
#897=FACE_OUTER_BOUND('',#1318,.T.);
#898=FACE_OUTER_BOUND('',#1319,.T.);
#899=FACE_OUTER_BOUND('',#1320,.T.);
#900=FACE_OUTER_BOUND('',#1321,.T.);
#901=FACE_OUTER_BOUND('',#1322,.T.);
#902=FACE_OUTER_BOUND('',#1324,.T.);
#903=FACE_OUTER_BOUND('',#1325,.T.);
#904=FACE_OUTER_BOUND('',#1326,.T.);
#905=FACE_OUTER_BOUND('',#1327,.T.);
#1315=EDGE_LOOP('',(#5117,#5118,#5119,#5120));
#1316=EDGE_LOOP('',(#5121,#5122,#5123,#5124));
#1317=EDGE_LOOP('',(#5125,#5126,#5127,#5128));
#1318=EDGE_LOOP('',(#5129,#5130,#5131,#5132));
#1319=EDGE_LOOP('',(#5133,#5134,#5135,#5136));
#1320=EDGE_LOOP('',(#5137,#5138,#5139,#5140));
#1321=EDGE_LOOP('',(#5141,#5142,#5143,#5144,#5145,#5146));
#1322=EDGE_LOOP('',(#5147));
#1323=EDGE_LOOP('',(#5148,#5149,#5150,#5151,#5152,#5153));
#1324=EDGE_LOOP('',(#5154,#5155,#5156,#5157));
#1325=EDGE_LOOP('',(#5158,#5159,#5160,#5161));
#1326=EDGE_LOOP('',(#5162,#5163,#5164,#5165));
#1327=EDGE_LOOP('',(#5166));
#1649=LINE('',#10850,#1991);
#1650=LINE('',#10852,#1992);
#1651=LINE('',#10854,#1993);
#1652=LINE('',#10855,#1994);
#1653=LINE('',#10858,#1995);
#1654=LINE('',#10860,#1996);
#1655=LINE('',#10861,#1997);
#1656=LINE('',#10864,#1998);
#1657=LINE('',#10866,#1999);
#1658=LINE('',#10867,#2000);
#1659=LINE('',#10870,#2001);
#1660=LINE('',#10872,#2002);
#1661=LINE('',#10873,#2003);
#1662=LINE('',#10876,#2004);
#1663=LINE('',#10878,#2005);
#1664=LINE('',#10879,#2006);
#1665=LINE('',#10881,#2007);
#1666=LINE('',#10882,#2008);
#1667=LINE('',#10890,#2009);
#1668=LINE('',#10894,#2010);
#1669=LINE('',#10898,#2011);
#1991=VECTOR('',#8485,1.);
#1992=VECTOR('',#8486,1.);
#1993=VECTOR('',#8487,1.);
#1994=VECTOR('',#8488,1.);
#1995=VECTOR('',#8491,1.);
#1996=VECTOR('',#8492,1.);
#1997=VECTOR('',#8493,1.);
#1998=VECTOR('',#8496,1.);
#1999=VECTOR('',#8497,1.);
#2000=VECTOR('',#8498,1.);
#2001=VECTOR('',#8501,1.);
#2002=VECTOR('',#8502,1.);
#2003=VECTOR('',#8503,1.);
#2004=VECTOR('',#8506,1.);
#2005=VECTOR('',#8507,1.);
#2006=VECTOR('',#8508,1.);
#2007=VECTOR('',#8511,1.);
#2008=VECTOR('',#8512,1.);
#2009=VECTOR('',#8523,0.235);
#2010=VECTOR('',#8528,0.25);
#2011=VECTOR('',#8533,0.2125);
#2379=CIRCLE('',#6670,0.22);
#2380=CIRCLE('',#6672,0.24505);
#2381=CIRCLE('',#6674,0.24505);
#2382=CIRCLE('',#6676,0.175);
#2880=VERTEX_POINT('',#10848);
#2881=VERTEX_POINT('',#10849);
#2882=VERTEX_POINT('',#10851);
#2883=VERTEX_POINT('',#10853);
#2884=VERTEX_POINT('',#10857);
#2885=VERTEX_POINT('',#10859);
#2886=VERTEX_POINT('',#10863);
#2887=VERTEX_POINT('',#10865);
#2888=VERTEX_POINT('',#10869);
#2889=VERTEX_POINT('',#10871);
#2890=VERTEX_POINT('',#10875);
#2891=VERTEX_POINT('',#10877);
#2892=VERTEX_POINT('',#10885);
#2893=VERTEX_POINT('',#10888);
#2894=VERTEX_POINT('',#10892);
#2895=VERTEX_POINT('',#10896);
#3628=EDGE_CURVE('',#2880,#2881,#1649,.T.);
#3629=EDGE_CURVE('',#2880,#2882,#1650,.T.);
#3630=EDGE_CURVE('',#2882,#2883,#1651,.T.);
#3631=EDGE_CURVE('',#2881,#2883,#1652,.T.);
#3632=EDGE_CURVE('',#2884,#2880,#1653,.T.);
#3633=EDGE_CURVE('',#2884,#2885,#1654,.T.);
#3634=EDGE_CURVE('',#2885,#2882,#1655,.T.);
#3635=EDGE_CURVE('',#2886,#2884,#1656,.T.);
#3636=EDGE_CURVE('',#2886,#2887,#1657,.T.);
#3637=EDGE_CURVE('',#2887,#2885,#1658,.T.);
#3638=EDGE_CURVE('',#2888,#2886,#1659,.T.);
#3639=EDGE_CURVE('',#2888,#2889,#1660,.T.);
#3640=EDGE_CURVE('',#2889,#2887,#1661,.T.);
#3641=EDGE_CURVE('',#2890,#2888,#1662,.T.);
#3642=EDGE_CURVE('',#2890,#2891,#1663,.T.);
#3643=EDGE_CURVE('',#2891,#2889,#1664,.T.);
#3644=EDGE_CURVE('',#2881,#2890,#1665,.T.);
#3645=EDGE_CURVE('',#2883,#2891,#1666,.T.);
#3646=EDGE_CURVE('',#2892,#2892,#2379,.T.);
#3647=EDGE_CURVE('',#2893,#2893,#2380,.T.);
#3648=EDGE_CURVE('',#2893,#2892,#1667,.T.);
#3649=EDGE_CURVE('',#2894,#2894,#2381,.F.);
#3650=EDGE_CURVE('',#2894,#2893,#1668,.T.);
#3651=EDGE_CURVE('',#2895,#2895,#2382,.T.);
#3652=EDGE_CURVE('',#2895,#2894,#1669,.T.);
#5117=ORIENTED_EDGE('',*,*,#3628,.F.);
#5118=ORIENTED_EDGE('',*,*,#3629,.T.);
#5119=ORIENTED_EDGE('',*,*,#3630,.T.);
#5120=ORIENTED_EDGE('',*,*,#3631,.F.);
#5121=ORIENTED_EDGE('',*,*,#3632,.F.);
#5122=ORIENTED_EDGE('',*,*,#3633,.T.);
#5123=ORIENTED_EDGE('',*,*,#3634,.T.);
#5124=ORIENTED_EDGE('',*,*,#3629,.F.);
#5125=ORIENTED_EDGE('',*,*,#3635,.F.);
#5126=ORIENTED_EDGE('',*,*,#3636,.T.);
#5127=ORIENTED_EDGE('',*,*,#3637,.T.);
#5128=ORIENTED_EDGE('',*,*,#3633,.F.);
#5129=ORIENTED_EDGE('',*,*,#3638,.F.);
#5130=ORIENTED_EDGE('',*,*,#3639,.T.);
#5131=ORIENTED_EDGE('',*,*,#3640,.T.);
#5132=ORIENTED_EDGE('',*,*,#3636,.F.);
#5133=ORIENTED_EDGE('',*,*,#3641,.F.);
#5134=ORIENTED_EDGE('',*,*,#3642,.T.);
#5135=ORIENTED_EDGE('',*,*,#3643,.T.);
#5136=ORIENTED_EDGE('',*,*,#3639,.F.);
#5137=ORIENTED_EDGE('',*,*,#3644,.F.);
#5138=ORIENTED_EDGE('',*,*,#3631,.T.);
#5139=ORIENTED_EDGE('',*,*,#3645,.T.);
#5140=ORIENTED_EDGE('',*,*,#3642,.F.);
#5141=ORIENTED_EDGE('',*,*,#3645,.F.);
#5142=ORIENTED_EDGE('',*,*,#3630,.F.);
#5143=ORIENTED_EDGE('',*,*,#3634,.F.);
#5144=ORIENTED_EDGE('',*,*,#3637,.F.);
#5145=ORIENTED_EDGE('',*,*,#3640,.F.);
#5146=ORIENTED_EDGE('',*,*,#3643,.F.);
#5147=ORIENTED_EDGE('',*,*,#3646,.F.);
#5148=ORIENTED_EDGE('',*,*,#3628,.T.);
#5149=ORIENTED_EDGE('',*,*,#3644,.T.);
#5150=ORIENTED_EDGE('',*,*,#3641,.T.);
#5151=ORIENTED_EDGE('',*,*,#3638,.T.);
#5152=ORIENTED_EDGE('',*,*,#3635,.T.);
#5153=ORIENTED_EDGE('',*,*,#3632,.T.);
#5154=ORIENTED_EDGE('',*,*,#3647,.F.);
#5155=ORIENTED_EDGE('',*,*,#3648,.T.);
#5156=ORIENTED_EDGE('',*,*,#3646,.T.);
#5157=ORIENTED_EDGE('',*,*,#3648,.F.);
#5158=ORIENTED_EDGE('',*,*,#3649,.F.);
#5159=ORIENTED_EDGE('',*,*,#3650,.T.);
#5160=ORIENTED_EDGE('',*,*,#3647,.T.);
#5161=ORIENTED_EDGE('',*,*,#3650,.F.);
#5162=ORIENTED_EDGE('',*,*,#3651,.F.);
#5163=ORIENTED_EDGE('',*,*,#3652,.T.);
#5164=ORIENTED_EDGE('',*,*,#3649,.T.);
#5165=ORIENTED_EDGE('',*,*,#3652,.F.);
#5166=ORIENTED_EDGE('',*,*,#3651,.T.);
#5320=CYLINDRICAL_SURFACE('',#6673,0.24505);
#5638=ADVANCED_FACE('',(#894),#568,.F.);
#5639=ADVANCED_FACE('',(#895),#569,.F.);
#5640=ADVANCED_FACE('',(#896),#570,.F.);
#5641=ADVANCED_FACE('',(#897),#571,.F.);
#5642=ADVANCED_FACE('',(#898),#572,.F.);
#5643=ADVANCED_FACE('',(#899),#573,.F.);
#5644=ADVANCED_FACE('',(#900),#574,.F.);
#5645=ADVANCED_FACE('',(#901,#433),#575,.T.);
#5646=ADVANCED_FACE('',(#902),#235,.T.);
#5647=ADVANCED_FACE('',(#903),#5320,.T.);
#5648=ADVANCED_FACE('',(#904),#236,.T.);
#5649=ADVANCED_FACE('',(#905),#576,.T.);
#5681=CLOSED_SHELL('',(#5638,#5639,#5640,#5641,#5642,#5643,#5644,#5645,
#5646,#5647,#5648,#5649));
#6661=AXIS2_PLACEMENT_3D('',#10846,#8481,#8482);
#6662=AXIS2_PLACEMENT_3D('',#10847,#8483,#8484);
#6663=AXIS2_PLACEMENT_3D('',#10856,#8489,#8490);
#6664=AXIS2_PLACEMENT_3D('',#10862,#8494,#8495);
#6665=AXIS2_PLACEMENT_3D('',#10868,#8499,#8500);
#6666=AXIS2_PLACEMENT_3D('',#10874,#8504,#8505);
#6667=AXIS2_PLACEMENT_3D('',#10880,#8509,#8510);
#6668=AXIS2_PLACEMENT_3D('',#10883,#8513,#8514);
#6669=AXIS2_PLACEMENT_3D('',#10884,#8515,#8516);
#6670=AXIS2_PLACEMENT_3D('',#10886,#8517,#8518);
#6671=AXIS2_PLACEMENT_3D('',#10887,#8519,#8520);
#6672=AXIS2_PLACEMENT_3D('',#10889,#8521,#8522);
#6673=AXIS2_PLACEMENT_3D('',#10891,#8524,#8525);
#6674=AXIS2_PLACEMENT_3D('',#10893,#8526,#8527);
#6675=AXIS2_PLACEMENT_3D('',#10895,#8529,#8530);
#6676=AXIS2_PLACEMENT_3D('',#10897,#8531,#8532);
#6677=AXIS2_PLACEMENT_3D('',#10899,#8534,#8535);
#8481=DIRECTION('axis',(0.,0.,1.));
#8482=DIRECTION('refdir',(1.,0.,0.));
#8483=DIRECTION('center_axis',(0.866025403784439,0.,-0.5));
#8484=DIRECTION('ref_axis',(0.5,0.,0.866025403784439));
#8485=DIRECTION('',(0.5,0.,0.866025403784439));
#8486=DIRECTION('',(0.,-1.,0.));
#8487=DIRECTION('',(0.5,0.,0.866025403784439));
#8488=DIRECTION('',(0.,-1.,0.));
#8489=DIRECTION('center_axis',(1.92296268638356E-16,0.,-1.));
#8490=DIRECTION('ref_axis',(1.,0.,1.92296268638356E-16));
#8491=DIRECTION('',(1.,0.,1.92296268638356E-16));
#8492=DIRECTION('',(0.,-1.,0.));
#8493=DIRECTION('',(1.,0.,1.92296268638356E-16));
#8494=DIRECTION('center_axis',(-0.866025403784439,0.,-0.5));
#8495=DIRECTION('ref_axis',(0.5,0.,-0.866025403784439));
#8496=DIRECTION('',(0.5,0.,-0.866025403784439));
#8497=DIRECTION('',(0.,-1.,0.));
#8498=DIRECTION('',(0.5,0.,-0.866025403784438));
#8499=DIRECTION('center_axis',(-0.866025403784439,0.,0.5));
#8500=DIRECTION('ref_axis',(-0.5,0.,-0.866025403784439));
#8501=DIRECTION('',(-0.5,0.,-0.866025403784439));
#8502=DIRECTION('',(0.,-1.,0.));
#8503=DIRECTION('',(-0.5,0.,-0.866025403784439));
#8504=DIRECTION('center_axis',(-1.92296268638356E-16,0.,1.));
#8505=DIRECTION('ref_axis',(-1.,0.,-1.92296268638356E-16));
#8506=DIRECTION('',(-1.,0.,-1.92296268638356E-16));
#8507=DIRECTION('',(0.,-1.,0.));
#8508=DIRECTION('',(-1.,0.,-1.92296268638356E-16));
#8509=DIRECTION('center_axis',(0.866025403784439,0.,0.5));
#8510=DIRECTION('ref_axis',(-0.5,0.,0.866025403784439));
#8511=DIRECTION('',(-0.5,0.,0.866025403784439));
#8512=DIRECTION('',(-0.5,0.,0.866025403784439));
#8513=DIRECTION('center_axis',(0.,-1.,0.));
#8514=DIRECTION('ref_axis',(0.,0.,-1.));
#8515=DIRECTION('center_axis',(0.,1.,0.));
#8516=DIRECTION('ref_axis',(0.,0.,1.));
#8517=DIRECTION('center_axis',(0.,-1.,0.));
#8518=DIRECTION('ref_axis',(1.,0.,0.));
#8519=DIRECTION('center_axis',(0.,-1.,0.));
#8520=DIRECTION('ref_axis',(1.,0.,0.));
#8521=DIRECTION('center_axis',(0.,-1.,0.));
#8522=DIRECTION('ref_axis',(1.,0.,0.));
#8523=DIRECTION('',(0.707106781186547,0.707106781186548,8.65956056235493E-17));
#8524=DIRECTION('center_axis',(0.,-1.,0.));
#8525=DIRECTION('ref_axis',(1.,0.,0.));
#8526=DIRECTION('center_axis',(0.,1.,0.));
#8527=DIRECTION('ref_axis',(1.,0.,0.));
#8528=DIRECTION('',(0.,1.,0.));
#8529=DIRECTION('center_axis',(0.,1.,0.));
#8530=DIRECTION('ref_axis',(1.,0.,0.));
#8531=DIRECTION('center_axis',(0.,-1.,0.));
#8532=DIRECTION('ref_axis',(1.,0.,0.));
#8533=DIRECTION('',(-0.707106781186547,0.707106781186548,-8.65956056235493E-17));
#8534=DIRECTION('center_axis',(0.,-1.,0.));
#8535=DIRECTION('ref_axis',(0.,0.,-1.));
#10846=CARTESIAN_POINT('',(0.,0.,0.));
#10847=CARTESIAN_POINT('Origin',(0.0721687836487032,0.,-0.125));
#10848=CARTESIAN_POINT('',(0.0721687836487032,0.,-0.125));
#10849=CARTESIAN_POINT('',(0.144337567297406,0.,0.));
#10850=CARTESIAN_POINT('',(0.117710979560879,0.,-0.0461186027918559));
#10851=CARTESIAN_POINT('',(0.0721687836487032,-0.25,-0.125));
#10852=CARTESIAN_POINT('',(0.0721687836487032,0.,-0.125));
#10853=CARTESIAN_POINT('',(0.144337567297406,-0.25,0.));
#10854=CARTESIAN_POINT('',(0.144337567297406,-0.25,0.));
#10855=CARTESIAN_POINT('',(0.144337567297406,0.,0.));
#10856=CARTESIAN_POINT('Origin',(-0.0721687836487032,0.,-0.125));
#10857=CARTESIAN_POINT('',(-0.0721687836487032,0.,-0.125));
#10858=CARTESIAN_POINT('',(0.0739156081756484,0.,-0.125));
#10859=CARTESIAN_POINT('',(-0.0721687836487032,-0.25,-0.125));
#10860=CARTESIAN_POINT('',(-0.0721687836487032,0.,-0.125));
#10861=CARTESIAN_POINT('',(0.0721687836487032,-0.25,-0.125));
#10862=CARTESIAN_POINT('Origin',(-0.144337567297406,0.,-4.16333634234434E-17));
#10863=CARTESIAN_POINT('',(-0.144337567297406,0.,-1.76762539787485E-17));
#10864=CARTESIAN_POINT('',(-0.0987953713852306,0.,-0.0788813972081442));
#10865=CARTESIAN_POINT('',(-0.144337567297406,-0.25,-2.77555756156289E-17));
#10866=CARTESIAN_POINT('',(-0.144337567297406,0.,-1.76762539787485E-17));
#10867=CARTESIAN_POINT('',(-0.0721687836487032,-0.25,-0.125));
#10868=CARTESIAN_POINT('Origin',(-0.0721687836487033,0.,0.125));
#10869=CARTESIAN_POINT('',(-0.0721687836487033,0.,0.125));
#10870=CARTESIAN_POINT('',(-0.0627109795608791,0.,0.141381397208144));
#10871=CARTESIAN_POINT('',(-0.0721687836487033,-0.25,0.125));
#10872=CARTESIAN_POINT('',(-0.0721687836487033,0.,0.125));
#10873=CARTESIAN_POINT('',(-0.144337567297406,-0.25,-1.76762539787485E-17));
#10874=CARTESIAN_POINT('Origin',(0.0721687836487032,0.,0.125));
#10875=CARTESIAN_POINT('',(0.0721687836487032,0.,0.125));
#10876=CARTESIAN_POINT('',(0.146084391824352,0.,0.125));
#10877=CARTESIAN_POINT('',(0.0721687836487032,-0.25,0.125));
#10878=CARTESIAN_POINT('',(0.0721687836487032,0.,0.125));
#10879=CARTESIAN_POINT('',(-0.0721687836487033,-0.25,0.125));
#10880=CARTESIAN_POINT('Origin',(0.144337567297406,0.,0.));
#10881=CARTESIAN_POINT('',(0.153795371385231,0.,-0.0163813972081441));
#10882=CARTESIAN_POINT('',(0.0721687836487032,-0.25,0.125));
#10883=CARTESIAN_POINT('Origin',(0.,-0.25,0.));
#10884=CARTESIAN_POINT('Origin',(0.22,0.,0.));
#10885=CARTESIAN_POINT('',(-0.22,-8.67361737988404E-18,-2.69422295812418E-17));
#10886=CARTESIAN_POINT('Origin',(0.,0.,0.));
#10887=CARTESIAN_POINT('Origin',(0.,-0.015,0.));
#10888=CARTESIAN_POINT('',(-0.24505,-0.02505,-3.00099698131059E-17));
#10889=CARTESIAN_POINT('Origin',(0.,-0.02505,0.));
#10890=CARTESIAN_POINT('',(-0.235,-0.015,-2.87791997799628E-17));
#10891=CARTESIAN_POINT('Origin',(0.,-0.3775,0.));
#10892=CARTESIAN_POINT('',(-0.24505,-0.72995,3.00099698131059E-17));
#10893=CARTESIAN_POINT('Origin',(0.,-0.72995,0.));
#10894=CARTESIAN_POINT('',(-0.24505,-0.3775,-3.00099698131059E-17));
#10895=CARTESIAN_POINT('Origin',(0.,-0.7625,0.));
#10896=CARTESIAN_POINT('',(-0.175,-0.8,-2.14313189850787E-17));
#10897=CARTESIAN_POINT('Origin',(0.,-0.8,0.));
#10898=CARTESIAN_POINT('',(-0.2125,-0.7625,-2.60237444818813E-17));
#10899=CARTESIAN_POINT('Origin',(0.,-0.8,0.));
#10935=UNCERTAINTY_MEASURE_WITH_UNIT(LENGTH_MEASURE(0.001),#10964,
'DISTANCE_ACCURACY_VALUE',
'Maximum model space distance between geometric entities at asserted c
onnectivities');
#10936=UNCERTAINTY_MEASURE_WITH_UNIT(LENGTH_MEASURE(0.001),#10964,
'DISTANCE_ACCURACY_VALUE',
'Maximum model space distance between geometric entities at asserted c
onnectivities');
#10962=(
GEOMETRIC_REPRESENTATION_CONTEXT(3)
GLOBAL_UNCERTAINTY_ASSIGNED_CONTEXT((#10935))
GLOBAL_UNIT_ASSIGNED_CONTEXT((#10964,#10966,#10967))
REPRESENTATION_CONTEXT('','3D')
);
#10963=(
GEOMETRIC_REPRESENTATION_CONTEXT(3)
GLOBAL_UNCERTAINTY_ASSIGNED_CONTEXT((#10936))
GLOBAL_UNIT_ASSIGNED_CONTEXT((#10964,#10966,#10967))
REPRESENTATION_CONTEXT('','3D')
);
#10964=(
LENGTH_UNIT()
NAMED_UNIT(*)
SI_UNIT(.CENTI.,.METRE.)
);
#10966=(
NAMED_UNIT(*)
PLANE_ANGLE_UNIT()
SI_UNIT($,.RADIAN.)
);
#10967=(
NAMED_UNIT(*)
SI_UNIT($,.STERADIAN.)
SOLID_ANGLE_UNIT()
);
#10993=SHAPE_DEFINITION_REPRESENTATION(#11046,#11082);
#11046=PRODUCT_DEFINITION_SHAPE('',$,#11109);
#11082=SHAPE_REPRESENTATION('',(#6661),#10962);
#11083=PRODUCT_DEFINITION_CONTEXT('part definition',#11163,'design');
#11109=PRODUCT_DEFINITION('Socket Set Screw - M5x8',
'Socket Set Screw - M5x8',#11135,#11083);
#11135=PRODUCT_DEFINITION_FORMATION('',$,#11190);
#11163=APPLICATION_CONTEXT(
'Core Data for Automotive Mechanical Design Process');
#11164=PRODUCT_CONTEXT('part definition',#11163,'mechanical');
#11190=PRODUCT('Socket Set Screw - M5x8','Socket Set Screw - M5x8',
'Socket Set Screw - M5x8',(#11164));
#11254=COLOUR_RGB('Black',0.12,0.14,0.17);
#11255=FILL_AREA_STYLE_COLOUR('',#11254);
#11256=FILL_AREA_STYLE('',(#11255));
#11257=SURFACE_STYLE_FILL_AREA(#11256);
#11258=SURFACE_SIDE_STYLE('',(#11257));
#11259=SURFACE_STYLE_USAGE(.BOTH.,#11258);
#11260=PRESENTATION_STYLE_ASSIGNMENT((#11259));
ENDSEC;
END-ISO-10303-21;
